ISO-10303-21;
HEADER;
/* Generated by software containing ST-Developer
 * from STEP Tools, Inc. (www.steptools.com) 
 */

FILE_DESCRIPTION(
/* description */ ('Flywheel Crank-Slider'),
/* implementation_level */ '2;1');

FILE_NAME(
/* name */ 'Bearing bolt reducer.step',
/* time_stamp */ '2026-10-28T03:23:13-07:00',
/* author */ (''),
/* organization */ (''),
/* preprocessor_version */ 'ST-DEVELOPER v20.2',
/* originating_system */ 'Autodesk Translation Framework v15.17.0.0',
/* authorisation */ '');

FILE_SCHEMA (('AUTOMOTIVE_DESIGN { 1 0 10303 214 3 1 1 }'));
ENDSEC;

DATA;
#10=MECHANICAL_DESIGN_GEOMETRIC_PRESENTATION_REPRESENTATION('',(#670),#17322);
#566=SHAPE_REPRESENTATION_RELATIONSHIP('SRR','None',#17562,#618);
#618=ADVANCED_BREP_SHAPE_REPRESENTATION('',(#731),#17266);
#670=STYLED_ITEM('',(#17938),#731);
#731=MANIFOLD_SOLID_BREP('Body1',#9048);
#823=FACE_BOUND('',#1936,.T.);
#824=FACE_BOUND('',#1938,.T.);
#1029=PLANE('',#9780);
#1030=PLANE('',#9781);
#1360=FACE_OUTER_BOUND('',#1933,.T.);
#1361=FACE_OUTER_BOUND('',#1934,.T.);
#1362=FACE_OUTER_BOUND('',#1935,.T.);
#1363=FACE_OUTER_BOUND('',#1937,.T.);
#1933=EDGE_LOOP('',(#6302,#6303,#6304,#6305));
#1934=EDGE_LOOP('',(#6306,#6307,#6308,#6309));
#1935=EDGE_LOOP('',(#6310));
#1936=EDGE_LOOP('',(#6311));
#1937=EDGE_LOOP('',(#6312));
#1938=EDGE_LOOP('',(#6313));
#2662=LINE('',#13930,#3273);
#2663=LINE('',#13936,#3274);
#3273=VECTOR('',#11058,0.425);
#3274=VECTOR('',#11065,0.645);
#3882=CIRCLE('',#9775,0.425);
#3883=CIRCLE('',#9776,0.425);
#3884=CIRCLE('',#9778,0.645);
#3885=CIRCLE('',#9779,0.645);
#4337=VERTEX_POINT('',#13927);
#4338=VERTEX_POINT('',#13929);
#4339=VERTEX_POINT('',#13933);
#4340=VERTEX_POINT('',#13935);
#5108=EDGE_CURVE('',#4337,#4337,#3882,.T.);
#5109=EDGE_CURVE('',#4337,#4338,#2662,.T.);
#5110=EDGE_CURVE('',#4338,#4338,#3883,.T.);
#5111=EDGE_CURVE('',#4339,#4339,#3884,.T.);
#5112=EDGE_CURVE('',#4339,#4340,#2663,.T.);
#5113=EDGE_CURVE('',#4340,#4340,#3885,.T.);
#6302=ORIENTED_EDGE('',*,*,#5108,.F.);
#6303=ORIENTED_EDGE('',*,*,#5109,.T.);
#6304=ORIENTED_EDGE('',*,*,#5110,.T.);
#6305=ORIENTED_EDGE('',*,*,#5109,.F.);
#6306=ORIENTED_EDGE('',*,*,#5111,.F.);
#6307=ORIENTED_EDGE('',*,*,#5112,.T.);
#6308=ORIENTED_EDGE('',*,*,#5113,.T.);
#6309=ORIENTED_EDGE('',*,*,#5112,.F.);
#6310=ORIENTED_EDGE('',*,*,#5111,.T.);
#6311=ORIENTED_EDGE('',*,*,#5108,.T.);
#6312=ORIENTED_EDGE('',*,*,#5113,.F.);
#6313=ORIENTED_EDGE('',*,*,#5110,.F.);
#8352=CYLINDRICAL_SURFACE('',#9774,0.425);
#8353=CYLINDRICAL_SURFACE('',#9777,0.645);
#8551=ADVANCED_FACE('',(#1360),#8352,.F.);
#8552=ADVANCED_FACE('',(#1361),#8353,.T.);
#8553=ADVANCED_FACE('',(#1362,#823),#1029,.T.);
#8554=ADVANCED_FACE('',(#1363,#824),#1030,.F.);
#9048=CLOSED_SHELL('',(#8551,#8552,#8553,#8554));
#9773=AXIS2_PLACEMENT_3D('',#13925,#11052,#11053);
#9774=AXIS2_PLACEMENT_3D('',#13926,#11054,#11055);
#9775=AXIS2_PLACEMENT_3D('',#13928,#11056,#11057);
#9776=AXIS2_PLACEMENT_3D('',#13931,#11059,#11060);
#9777=AXIS2_PLACEMENT_3D('',#13932,#11061,#11062);
#9778=AXIS2_PLACEMENT_3D('',#13934,#11063,#11064);
#9779=AXIS2_PLACEMENT_3D('',#13937,#11066,#11067);
#9780=AXIS2_PLACEMENT_3D('',#13938,#11068,#11069);
#9781=AXIS2_PLACEMENT_3D('',#13939,#11070,#11071);
#11052=DIRECTION('axis',(0.,0.,1.));
#11053=DIRECTION('refdir',(1.,0.,0.));
#11054=DIRECTION('center_axis',(0.,0.,1.));
#11055=DIRECTION('ref_axis',(1.,0.,0.));
#11056=DIRECTION('center_axis',(0.,0.,-1.));
#11057=DIRECTION('ref_axis',(1.,0.,0.));
#11058=DIRECTION('',(0.,0.,-1.));
#11059=DIRECTION('center_axis',(0.,0.,-1.));
#11060=DIRECTION('ref_axis',(1.,0.,0.));
#11061=DIRECTION('center_axis',(0.,0.,1.));
#11062=DIRECTION('ref_axis',(1.,0.,0.));
#11063=DIRECTION('center_axis',(0.,0.,1.));
#11064=DIRECTION('ref_axis',(1.,0.,0.));
#11065=DIRECTION('',(0.,0.,-1.));
#11066=DIRECTION('center_axis',(0.,0.,1.));
#11067=DIRECTION('ref_axis',(1.,0.,0.));
#11068=DIRECTION('center_axis',(0.,0.,1.));
#11069=DIRECTION('ref_axis',(1.,0.,0.));
#11070=DIRECTION('center_axis',(0.,0.,1.));
#11071=DIRECTION('ref_axis',(1.,0.,0.));
#13925=CARTESIAN_POINT('',(0.,0.,0.));
#13926=CARTESIAN_POINT('Origin',(-4.75,-15.,6.67));
#13927=CARTESIAN_POINT('',(-5.175,-15.,7.87));
#13928=CARTESIAN_POINT('Origin',(-4.75,-15.,7.87));
#13929=CARTESIAN_POINT('',(-5.175,-15.,6.67));
#13930=CARTESIAN_POINT('',(-5.175,-15.,6.67));
#13931=CARTESIAN_POINT('Origin',(-4.75,-15.,6.67));
#13932=CARTESIAN_POINT('Origin',(-4.75,-15.,6.67));
#13933=CARTESIAN_POINT('',(-5.395,-15.,7.87));
#13934=CARTESIAN_POINT('Origin',(-4.75,-15.,7.87));
#13935=CARTESIAN_POINT('',(-5.395,-15.,6.67));
#13936=CARTESIAN_POINT('',(-5.395,-15.,6.67));
#13937=CARTESIAN_POINT('Origin',(-4.75,-15.,6.67));
#13938=CARTESIAN_POINT('Origin',(-4.75,-15.,7.87));
#13939=CARTESIAN_POINT('Origin',(-4.75,-15.,6.67));
#17205=UNCERTAINTY_MEASURE_WITH_UNIT(LENGTH_MEASURE(0.001),#17323,
'DISTANCE_ACCURACY_VALUE',
'Maximum model space distance between geometric entities at asserted c
onnectivities');
#17261=UNCERTAINTY_MEASURE_WITH_UNIT(LENGTH_MEASURE(0.001),#17323,
'DISTANCE_ACCURACY_VALUE',
'Maximum model space distance between geometric entities at asserted c
onnectivities');
#17266=(
GEOMETRIC_REPRESENTATION_CONTEXT(3)
GLOBAL_UNCERTAINTY_ASSIGNED_CONTEXT((#17205))
GLOBAL_UNIT_ASSIGNED_CONTEXT((#17323,#17325,#17326))
REPRESENTATION_CONTEXT('','3D')
);
#17322=(
GEOMETRIC_REPRESENTATION_CONTEXT(3)
GLOBAL_UNCERTAINTY_ASSIGNED_CONTEXT((#17261))
GLOBAL_UNIT_ASSIGNED_CONTEXT((#17323,#17325,#17326))
REPRESENTATION_CONTEXT('','3D')
);
#17323=(
LENGTH_UNIT()
NAMED_UNIT(*)
SI_UNIT(.CENTI.,.METRE.)
);
#17325=(
NAMED_UNIT(*)
PLANE_ANGLE_UNIT()
SI_UNIT($,.RADIAN.)
);
#17326=(
NAMED_UNIT(*)
SI_UNIT($,.STERADIAN.)
SOLID_ANGLE_UNIT()
);
#17331=SHAPE_DEFINITION_REPRESENTATION(#17391,#17562);
#17391=PRODUCT_DEFINITION_SHAPE('',$,#17623);
#17562=SHAPE_REPRESENTATION('',(#9773),#17266);
#17618=PRODUCT_DEFINITION_CONTEXT('part definition',#17800,'design');
#17623=PRODUCT_DEFINITION('Bearing bolt reducer','Bearing bolt reducer',
#17683,#17618);
#17683=PRODUCT_DEFINITION_FORMATION('',$,#17806);
#17800=APPLICATION_CONTEXT(
'Core Data for Automotive Mechanical Design Process');
#17801=PRODUCT_CONTEXT('part definition',#17800,'mechanical');
#17806=PRODUCT('Bearing bolt reducer','Bearing bolt reducer',
'Bearing bolt reducer',(#17801));
#17932=COLOUR_RGB('Black',0.12,0.14,0.17);
#17933=FILL_AREA_STYLE_COLOUR('',#17932);
#17934=FILL_AREA_STYLE('',(#17933));
#17935=SURFACE_STYLE_FILL_AREA(#17934);
#17936=SURFACE_SIDE_STYLE('',(#17935));
#17937=SURFACE_STYLE_USAGE(.BOTH.,#17936);
#17938=PRESENTATION_STYLE_ASSIGNMENT((#17937));
ENDSEC;
END-ISO-10303-21;
